ISO-10303-21;
HEADER;
/* Generated by software containing ST-Developer
 * from STEP Tools, Inc. (www.steptools.com) 
 */

FILE_DESCRIPTION(
/* description */ ('Rack and pinion manual slide'),
/* implementation_level */ '2;1');

FILE_NAME(
/* name */ 'M4x10 Cap Screw.step',
/* time_stamp */ '2026-10-28T03:22:49-07:00',
/* author */ (''),
/* organization */ (''),
/* preprocessor_version */ 'ST-DEVELOPER v20.2',
/* originating_system */ 'Autodesk Translation Framework v15.17.0.0',
/* authorisation */ '');

FILE_SCHEMA (('AUTOMOTIVE_DESIGN { 1 0 10303 214 3 1 1 }'));
ENDSEC;

DATA;
#10=MECHANICAL_DESIGN_GEOMETRIC_PRESENTATION_REPRESENTATION('',(#763),#34851);
#606=ORIENTED_CLOSED_SHELL('',*,#13784,.F.);
#611=BREP_WITH_VOIDS('Body1',#13785,(#606));
#624=CONICAL_SURFACE('',#14919,0.325,0.785398163397448);
#625=CONICAL_SURFACE('',#14923,0.335,0.785398163397448);
#626=CONICAL_SURFACE('',#14927,0.21,0.463647609000806);
#664=SHAPE_REPRESENTATION_RELATIONSHIP('SRR','None',#35100,#710);
#710=ADVANCED_BREP_SHAPE_REPRESENTATION('',(#611),#34825);
#763=STYLED_ITEM('',(#35418),#611);
#984=FACE_BOUND('',#2750,.T.);
#1234=PLANE('',#14907);
#1235=PLANE('',#14908);
#1236=PLANE('',#14909);
#1237=PLANE('',#14910);
#1238=PLANE('',#14911);
#1239=PLANE('',#14912);
#1240=PLANE('',#14913);
#1241=PLANE('',#14914);
#1242=PLANE('',#14915);
#1243=PLANE('',#14917);
#1244=PLANE('',#14925);
#1846=FACE_OUTER_BOUND('',#2736,.T.);
#1847=FACE_OUTER_BOUND('',#2737,.T.);
#1848=FACE_OUTER_BOUND('',#2738,.T.);
#1849=FACE_OUTER_BOUND('',#2739,.T.);
#1850=FACE_OUTER_BOUND('',#2740,.T.);
#1851=FACE_OUTER_BOUND('',#2741,.T.);
#1852=FACE_OUTER_BOUND('',#2742,.T.);
#1853=FACE_OUTER_BOUND('',#2743,.T.);
#1854=FACE_OUTER_BOUND('',#2744,.T.);
#1855=FACE_OUTER_BOUND('',#2745,.T.);
#1856=FACE_OUTER_BOUND('',#2746,.T.);
#1857=FACE_OUTER_BOUND('',#2747,.T.);
#1858=FACE_OUTER_BOUND('',#2748,.T.);
#1859=FACE_OUTER_BOUND('',#2749,.T.);
#1860=FACE_OUTER_BOUND('',#2751,.T.);
#1861=FACE_OUTER_BOUND('',#2752,.T.);
#2736=EDGE_LOOP('',(#10688,#10689,#10690,#10691));
#2737=EDGE_LOOP('',(#10692,#10693,#10694,#10695));
#2738=EDGE_LOOP('',(#10696,#10697,#10698,#10699));
#2739=EDGE_LOOP('',(#10700,#10701,#10702,#10703));
#2740=EDGE_LOOP('',(#10704,#10705,#10706,#10707));
#2741=EDGE_LOOP('',(#10708,#10709,#10710,#10711));
#2742=EDGE_LOOP('',(#10712,#10713,#10714,#10715,#10716,#10717));
#2743=EDGE_LOOP('',(#10718,#10719,#10720,#10721,#10722,#10723));
#2744=EDGE_LOOP('',(#10724));
#2745=EDGE_LOOP('',(#10725));
#2746=EDGE_LOOP('',(#10726,#10727,#10728,#10729));
#2747=EDGE_LOOP('',(#10730,#10731,#10732,#10733));
#2748=EDGE_LOOP('',(#10734,#10735,#10736,#10737));
#2749=EDGE_LOOP('',(#10738));
#2750=EDGE_LOOP('',(#10739));
#2751=EDGE_LOOP('',(#10740,#10741,#10742,#10743));
#2752=EDGE_LOOP('',(#10744,#10745,#10746,#10747));
#3691=LINE('',#21316,#4982);
#3692=LINE('',#21318,#4983);
#3693=LINE('',#21320,#4984);
#3694=LINE('',#21321,#4985);
#3695=LINE('',#21324,#4986);
#3696=LINE('',#21326,#4987);
#3697=LINE('',#21327,#4988);
#3698=LINE('',#21330,#4989);
#3699=LINE('',#21332,#4990);
#3700=LINE('',#21333,#4991);
#3701=LINE('',#21336,#4992);
#3702=LINE('',#21338,#4993);
#3703=LINE('',#21339,#4994);
#3704=LINE('',#21342,#4995);
#3705=LINE('',#21344,#4996);
#3706=LINE('',#21345,#4997);
#3707=LINE('',#21347,#4998);
#3708=LINE('',#21348,#4999);
#3709=LINE('',#21360,#5000);
#3710=LINE('',#21364,#5001);
#3711=LINE('',#21368,#5002);
#3712=LINE('',#21375,#5003);
#3713=LINE('',#21377,#5004);
#4982=VECTOR('',#17249,1.);
#4983=VECTOR('',#17250,1.);
#4984=VECTOR('',#17251,1.);
#4985=VECTOR('',#17252,1.);
#4986=VECTOR('',#17255,1.);
#4987=VECTOR('',#17256,1.);
#4988=VECTOR('',#17257,1.);
#4989=VECTOR('',#17260,1.);
#4990=VECTOR('',#17261,1.);
#4991=VECTOR('',#17262,1.);
#4992=VECTOR('',#17265,1.);
#4993=VECTOR('',#17266,1.);
#4994=VECTOR('',#17267,1.);
#4995=VECTOR('',#17270,1.);
#4996=VECTOR('',#17271,1.);
#4997=VECTOR('',#17272,1.);
#4998=VECTOR('',#17275,1.);
#4999=VECTOR('',#17276,1.);
#5000=VECTOR('',#17293,0.325);
#5001=VECTOR('',#17298,0.35);
#5002=VECTOR('',#17303,0.335);
#5003=VECTOR('',#17312,0.21);
#5004=VECTOR('',#17315,0.2);
#6050=CIRCLE('',#14916,0.1954);
#6051=CIRCLE('',#14918,0.3);
#6052=CIRCLE('',#14920,0.35);
#6053=CIRCLE('',#14922,0.35);
#6054=CIRCLE('',#14924,0.32);
#6055=CIRCLE('',#14926,0.22);
#6056=CIRCLE('',#14928,0.1954);
#6715=VERTEX_POINT('',#21314);
#6716=VERTEX_POINT('',#21315);
#6717=VERTEX_POINT('',#21317);
#6718=VERTEX_POINT('',#21319);
#6719=VERTEX_POINT('',#21323);
#6720=VERTEX_POINT('',#21325);
#6721=VERTEX_POINT('',#21329);
#6722=VERTEX_POINT('',#21331);
#6723=VERTEX_POINT('',#21335);
#6724=VERTEX_POINT('',#21337);
#6725=VERTEX_POINT('',#21341);
#6726=VERTEX_POINT('',#21343);
#6727=VERTEX_POINT('',#21352);
#6728=VERTEX_POINT('',#21355);
#6729=VERTEX_POINT('',#21358);
#6730=VERTEX_POINT('',#21362);
#6731=VERTEX_POINT('',#21366);
#6732=VERTEX_POINT('',#21370);
#6733=VERTEX_POINT('',#21373);
#8156=EDGE_CURVE('',#6715,#6716,#3691,.T.);
#8157=EDGE_CURVE('',#6716,#6717,#3692,.T.);
#8158=EDGE_CURVE('',#6717,#6718,#3693,.T.);
#8159=EDGE_CURVE('',#6715,#6718,#3694,.T.);
#8160=EDGE_CURVE('',#6716,#6719,#3695,.T.);
#8161=EDGE_CURVE('',#6719,#6720,#3696,.T.);
#8162=EDGE_CURVE('',#6720,#6717,#3697,.T.);
#8163=EDGE_CURVE('',#6719,#6721,#3698,.T.);
#8164=EDGE_CURVE('',#6721,#6722,#3699,.T.);
#8165=EDGE_CURVE('',#6722,#6720,#3700,.T.);
#8166=EDGE_CURVE('',#6721,#6723,#3701,.T.);
#8167=EDGE_CURVE('',#6723,#6724,#3702,.T.);
#8168=EDGE_CURVE('',#6724,#6722,#3703,.T.);
#8169=EDGE_CURVE('',#6723,#6725,#3704,.T.);
#8170=EDGE_CURVE('',#6725,#6726,#3705,.T.);
#8171=EDGE_CURVE('',#6726,#6724,#3706,.T.);
#8172=EDGE_CURVE('',#6725,#6715,#3707,.T.);
#8173=EDGE_CURVE('',#6718,#6726,#3708,.T.);
#8174=EDGE_CURVE('',#6727,#6727,#6050,.T.);
#8175=EDGE_CURVE('',#6728,#6728,#6051,.T.);
#8176=EDGE_CURVE('',#6729,#6729,#6052,.T.);
#8177=EDGE_CURVE('',#6729,#6728,#3709,.T.);
#8178=EDGE_CURVE('',#6730,#6730,#6053,.T.);
#8179=EDGE_CURVE('',#6730,#6729,#3710,.T.);
#8180=EDGE_CURVE('',#6731,#6731,#6054,.T.);
#8181=EDGE_CURVE('',#6731,#6730,#3711,.T.);
#8182=EDGE_CURVE('',#6732,#6732,#6055,.T.);
#8183=EDGE_CURVE('',#6733,#6733,#6056,.F.);
#8184=EDGE_CURVE('',#6733,#6732,#3712,.T.);
#8185=EDGE_CURVE('',#6727,#6733,#3713,.T.);
#10688=ORIENTED_EDGE('',*,*,#8156,.T.);
#10689=ORIENTED_EDGE('',*,*,#8157,.T.);
#10690=ORIENTED_EDGE('',*,*,#8158,.T.);
#10691=ORIENTED_EDGE('',*,*,#8159,.F.);
#10692=ORIENTED_EDGE('',*,*,#8160,.T.);
#10693=ORIENTED_EDGE('',*,*,#8161,.T.);
#10694=ORIENTED_EDGE('',*,*,#8162,.T.);
#10695=ORIENTED_EDGE('',*,*,#8157,.F.);
#10696=ORIENTED_EDGE('',*,*,#8163,.T.);
#10697=ORIENTED_EDGE('',*,*,#8164,.T.);
#10698=ORIENTED_EDGE('',*,*,#8165,.T.);
#10699=ORIENTED_EDGE('',*,*,#8161,.F.);
#10700=ORIENTED_EDGE('',*,*,#8166,.T.);
#10701=ORIENTED_EDGE('',*,*,#8167,.T.);
#10702=ORIENTED_EDGE('',*,*,#8168,.T.);
#10703=ORIENTED_EDGE('',*,*,#8164,.F.);
#10704=ORIENTED_EDGE('',*,*,#8169,.T.);
#10705=ORIENTED_EDGE('',*,*,#8170,.T.);
#10706=ORIENTED_EDGE('',*,*,#8171,.T.);
#10707=ORIENTED_EDGE('',*,*,#8167,.F.);
#10708=ORIENTED_EDGE('',*,*,#8172,.T.);
#10709=ORIENTED_EDGE('',*,*,#8159,.T.);
#10710=ORIENTED_EDGE('',*,*,#8173,.T.);
#10711=ORIENTED_EDGE('',*,*,#8170,.F.);
#10712=ORIENTED_EDGE('',*,*,#8172,.F.);
#10713=ORIENTED_EDGE('',*,*,#8169,.F.);
#10714=ORIENTED_EDGE('',*,*,#8166,.F.);
#10715=ORIENTED_EDGE('',*,*,#8163,.F.);
#10716=ORIENTED_EDGE('',*,*,#8160,.F.);
#10717=ORIENTED_EDGE('',*,*,#8156,.F.);
#10718=ORIENTED_EDGE('',*,*,#8173,.F.);
#10719=ORIENTED_EDGE('',*,*,#8158,.F.);
#10720=ORIENTED_EDGE('',*,*,#8162,.F.);
#10721=ORIENTED_EDGE('',*,*,#8165,.F.);
#10722=ORIENTED_EDGE('',*,*,#8168,.F.);
#10723=ORIENTED_EDGE('',*,*,#8171,.F.);
#10724=ORIENTED_EDGE('',*,*,#8174,.F.);
#10725=ORIENTED_EDGE('',*,*,#8175,.F.);
#10726=ORIENTED_EDGE('',*,*,#8176,.F.);
#10727=ORIENTED_EDGE('',*,*,#8177,.T.);
#10728=ORIENTED_EDGE('',*,*,#8175,.T.);
#10729=ORIENTED_EDGE('',*,*,#8177,.F.);
#10730=ORIENTED_EDGE('',*,*,#8178,.F.);
#10731=ORIENTED_EDGE('',*,*,#8179,.T.);
#10732=ORIENTED_EDGE('',*,*,#8176,.T.);
#10733=ORIENTED_EDGE('',*,*,#8179,.F.);
#10734=ORIENTED_EDGE('',*,*,#8180,.F.);
#10735=ORIENTED_EDGE('',*,*,#8181,.T.);
#10736=ORIENTED_EDGE('',*,*,#8178,.T.);
#10737=ORIENTED_EDGE('',*,*,#8181,.F.);
#10738=ORIENTED_EDGE('',*,*,#8180,.T.);
#10739=ORIENTED_EDGE('',*,*,#8182,.F.);
#10740=ORIENTED_EDGE('',*,*,#8183,.F.);
#10741=ORIENTED_EDGE('',*,*,#8184,.T.);
#10742=ORIENTED_EDGE('',*,*,#8182,.T.);
#10743=ORIENTED_EDGE('',*,*,#8184,.F.);
#10744=ORIENTED_EDGE('',*,*,#8174,.T.);
#10745=ORIENTED_EDGE('',*,*,#8185,.T.);
#10746=ORIENTED_EDGE('',*,*,#8183,.T.);
#10747=ORIENTED_EDGE('',*,*,#8185,.F.);
#12940=CYLINDRICAL_SURFACE('',#14921,0.35);
#12941=CYLINDRICAL_SURFACE('',#14929,0.1954);
#13324=ADVANCED_FACE('',(#1846),#1234,.F.);
#13325=ADVANCED_FACE('',(#1847),#1235,.F.);
#13326=ADVANCED_FACE('',(#1848),#1236,.F.);
#13327=ADVANCED_FACE('',(#1849),#1237,.F.);
#13328=ADVANCED_FACE('',(#1850),#1238,.F.);
#13329=ADVANCED_FACE('',(#1851),#1239,.F.);
#13330=ADVANCED_FACE('',(#1852),#1240,.F.);
#13331=ADVANCED_FACE('',(#1853),#1241,.F.);
#13332=ADVANCED_FACE('',(#1854),#1242,.F.);
#13333=ADVANCED_FACE('',(#1855),#1243,.T.);
#13334=ADVANCED_FACE('',(#1856),#624,.T.);
#13335=ADVANCED_FACE('',(#1857),#12940,.T.);
#13336=ADVANCED_FACE('',(#1858),#625,.T.);
#13337=ADVANCED_FACE('',(#1859,#984),#1244,.T.);
#13338=ADVANCED_FACE('',(#1860),#626,.T.);
#13339=ADVANCED_FACE('',(#1861),#12941,.T.);
#13784=CLOSED_SHELL('',(#13324,#13325,#13326,#13327,#13328,#13329,#13330,
#13331));
#13785=CLOSED_SHELL('',(#13332,#13333,#13334,#13335,#13336,#13337,#13338,
#13339));
#14906=AXIS2_PLACEMENT_3D('',#21312,#17245,#17246);
#14907=AXIS2_PLACEMENT_3D('',#21313,#17247,#17248);
#14908=AXIS2_PLACEMENT_3D('',#21322,#17253,#17254);
#14909=AXIS2_PLACEMENT_3D('',#21328,#17258,#17259);
#14910=AXIS2_PLACEMENT_3D('',#21334,#17263,#17264);
#14911=AXIS2_PLACEMENT_3D('',#21340,#17268,#17269);
#14912=AXIS2_PLACEMENT_3D('',#21346,#17273,#17274);
#14913=AXIS2_PLACEMENT_3D('',#21349,#17277,#17278);
#14914=AXIS2_PLACEMENT_3D('',#21350,#17279,#17280);
#14915=AXIS2_PLACEMENT_3D('',#21351,#17281,#17282);
#14916=AXIS2_PLACEMENT_3D('',#21353,#17283,#17284);
#14917=AXIS2_PLACEMENT_3D('',#21354,#17285,#17286);
#14918=AXIS2_PLACEMENT_3D('',#21356,#17287,#17288);
#14919=AXIS2_PLACEMENT_3D('',#21357,#17289,#17290);
#14920=AXIS2_PLACEMENT_3D('',#21359,#17291,#17292);
#14921=AXIS2_PLACEMENT_3D('',#21361,#17294,#17295);
#14922=AXIS2_PLACEMENT_3D('',#21363,#17296,#17297);
#14923=AXIS2_PLACEMENT_3D('',#21365,#17299,#17300);
#14924=AXIS2_PLACEMENT_3D('',#21367,#17301,#17302);
#14925=AXIS2_PLACEMENT_3D('',#21369,#17304,#17305);
#14926=AXIS2_PLACEMENT_3D('',#21371,#17306,#17307);
#14927=AXIS2_PLACEMENT_3D('',#21372,#17308,#17309);
#14928=AXIS2_PLACEMENT_3D('',#21374,#17310,#17311);
#14929=AXIS2_PLACEMENT_3D('',#21376,#17313,#17314);
#17245=DIRECTION('axis',(0.,0.,1.));
#17246=DIRECTION('refdir',(1.,0.,0.));
#17247=DIRECTION('center_axis',(0.866025403784439,0.,-0.5));
#17248=DIRECTION('ref_axis',(0.5,0.,0.866025403784439));
#17249=DIRECTION('',(-0.5,0.,-0.866025403784439));
#17250=DIRECTION('',(0.,-1.,0.));
#17251=DIRECTION('',(0.5,0.,0.866025403784439));
#17252=DIRECTION('',(0.,-1.,0.));
#17253=DIRECTION('center_axis',(1.60246890531964E-16,0.,-1.));
#17254=DIRECTION('ref_axis',(1.,0.,1.60246890531964E-16));
#17255=DIRECTION('',(-1.,0.,-1.60246890531964E-16));
#17256=DIRECTION('',(0.,-1.,0.));
#17257=DIRECTION('',(1.,0.,1.60246890531964E-16));
#17258=DIRECTION('center_axis',(-0.866025403784439,0.,-0.5));
#17259=DIRECTION('ref_axis',(0.5,0.,-0.866025403784439));
#17260=DIRECTION('',(-0.5,0.,0.866025403784439));
#17261=DIRECTION('',(0.,-1.,0.));
#17262=DIRECTION('',(0.5,0.,-0.866025403784439));
#17263=DIRECTION('center_axis',(-0.866025403784439,0.,0.5));
#17264=DIRECTION('ref_axis',(-0.5,0.,-0.866025403784439));
#17265=DIRECTION('',(0.5,0.,0.866025403784439));
#17266=DIRECTION('',(0.,-1.,0.));
#17267=DIRECTION('',(-0.5,0.,-0.866025403784439));
#17268=DIRECTION('center_axis',(-1.60246890531964E-16,0.,1.));
#17269=DIRECTION('ref_axis',(-1.,0.,-1.60246890531964E-16));
#17270=DIRECTION('',(1.,0.,1.60246890531964E-16));
#17271=DIRECTION('',(0.,-1.,0.));
#17272=DIRECTION('',(-1.,0.,-1.60246890531964E-16));
#17273=DIRECTION('center_axis',(0.866025403784439,0.,0.5));
#17274=DIRECTION('ref_axis',(-0.5,0.,0.866025403784439));
#17275=DIRECTION('',(0.5,0.,-0.866025403784439));
#17276=DIRECTION('',(-0.5,0.,0.866025403784439));
#17277=DIRECTION('center_axis',(0.,1.,0.));
#17278=DIRECTION('ref_axis',(1.,0.,0.));
#17279=DIRECTION('center_axis',(0.,-1.,0.));
#17280=DIRECTION('ref_axis',(0.,0.,-1.));
#17281=DIRECTION('center_axis',(0.,1.,0.));
#17282=DIRECTION('ref_axis',(1.,0.,0.));
#17283=DIRECTION('center_axis',(0.,1.,0.));
#17284=DIRECTION('ref_axis',(1.,0.,0.));
#17285=DIRECTION('center_axis',(0.,1.,0.));
#17286=DIRECTION('ref_axis',(0.,0.,1.));
#17287=DIRECTION('center_axis',(0.,-1.,0.));
#17288=DIRECTION('ref_axis',(1.,0.,0.));
#17289=DIRECTION('center_axis',(0.,-1.,0.));
#17290=DIRECTION('ref_axis',(1.,0.,0.));
#17291=DIRECTION('center_axis',(0.,-1.,0.));
#17292=DIRECTION('ref_axis',(1.,0.,0.));
#17293=DIRECTION('',(0.707106781186547,0.707106781186548,8.65956056235493E-17));
#17294=DIRECTION('center_axis',(0.,-1.,0.));
#17295=DIRECTION('ref_axis',(1.,0.,0.));
#17296=DIRECTION('center_axis',(0.,-1.,0.));
#17297=DIRECTION('ref_axis',(1.,0.,0.));
#17298=DIRECTION('',(0.,1.,0.));
#17299=DIRECTION('center_axis',(0.,1.,0.));
#17300=DIRECTION('ref_axis',(1.,0.,0.));
#17301=DIRECTION('center_axis',(0.,-1.,0.));
#17302=DIRECTION('ref_axis',(1.,0.,0.));
#17303=DIRECTION('',(-0.707106781186547,0.707106781186548,-8.65956056235493E-17));
#17304=DIRECTION('center_axis',(0.,-1.,0.));
#17305=DIRECTION('ref_axis',(0.,0.,-1.));
#17306=DIRECTION('center_axis',(0.,-1.,0.));
#17307=DIRECTION('ref_axis',(1.,0.,0.));
#17308=DIRECTION('center_axis',(0.,1.,0.));
#17309=DIRECTION('ref_axis',(1.,0.,0.));
#17310=DIRECTION('center_axis',(0.,1.,0.));
#17311=DIRECTION('ref_axis',(1.,0.,0.));
#17312=DIRECTION('',(-0.447213595499958,0.894427190999916,-5.47678698264203E-17));
#17313=DIRECTION('center_axis',(0.,-1.,0.));
#17314=DIRECTION('ref_axis',(1.,0.,0.));
#17315=DIRECTION('',(0.,1.,0.));
#21312=CARTESIAN_POINT('',(0.,0.,0.));
#21313=CARTESIAN_POINT('Origin',(0.0866025403784439,-0.4,-0.15));
#21314=CARTESIAN_POINT('',(0.173205080756888,-0.4,0.));
#21315=CARTESIAN_POINT('',(0.0866025403784439,-0.4,-0.15));
#21316=CARTESIAN_POINT('',(0.173205080756888,-0.4,0.));
#21317=CARTESIAN_POINT('',(0.0866025403784439,-0.64,-0.15));
#21318=CARTESIAN_POINT('',(0.0866025403784439,-0.4,-0.15));
#21319=CARTESIAN_POINT('',(0.173205080756888,-0.64,0.));
#21320=CARTESIAN_POINT('',(0.173205080756888,-0.64,0.));
#21321=CARTESIAN_POINT('',(0.173205080756888,-0.4,0.));
#21322=CARTESIAN_POINT('Origin',(-0.0866025403784438,-0.4,-0.15));
#21323=CARTESIAN_POINT('',(-0.0866025403784438,-0.4,-0.15));
#21324=CARTESIAN_POINT('',(0.0866025403784439,-0.4,-0.15));
#21325=CARTESIAN_POINT('',(-0.0866025403784438,-0.64,-0.15));
#21326=CARTESIAN_POINT('',(-0.0866025403784438,-0.4,-0.15));
#21327=CARTESIAN_POINT('',(0.0866025403784439,-0.64,-0.15));
#21328=CARTESIAN_POINT('Origin',(-0.173205080756888,-0.4,-2.77555756156289E-17));
#21329=CARTESIAN_POINT('',(-0.173205080756888,-0.4,-2.12115047744981E-17));
#21330=CARTESIAN_POINT('',(-0.0866025403784438,-0.4,-0.15));
#21331=CARTESIAN_POINT('',(-0.173205080756888,-0.64,-2.77555756156289E-17));
#21332=CARTESIAN_POINT('',(-0.173205080756888,-0.4,-2.12115047744981E-17));
#21333=CARTESIAN_POINT('',(-0.0866025403784438,-0.64,-0.15));
#21334=CARTESIAN_POINT('Origin',(-0.0866025403784439,-0.4,0.15));
#21335=CARTESIAN_POINT('',(-0.0866025403784439,-0.4,0.15));
#21336=CARTESIAN_POINT('',(-0.173205080756888,-0.4,-2.12115047744981E-17));
#21337=CARTESIAN_POINT('',(-0.0866025403784439,-0.64,0.15));
#21338=CARTESIAN_POINT('',(-0.0866025403784439,-0.4,0.15));
#21339=CARTESIAN_POINT('',(-0.173205080756888,-0.64,-2.12115047744981E-17));
#21340=CARTESIAN_POINT('Origin',(0.0866025403784439,-0.4,0.15));
#21341=CARTESIAN_POINT('',(0.0866025403784439,-0.4,0.15));
#21342=CARTESIAN_POINT('',(-0.0866025403784439,-0.4,0.15));
#21343=CARTESIAN_POINT('',(0.0866025403784439,-0.64,0.15));
#21344=CARTESIAN_POINT('',(0.0866025403784439,-0.4,0.15));
#21345=CARTESIAN_POINT('',(-0.0866025403784439,-0.64,0.15));
#21346=CARTESIAN_POINT('Origin',(0.173205080756888,-0.4,0.));
#21347=CARTESIAN_POINT('',(0.0866025403784439,-0.4,0.15));
#21348=CARTESIAN_POINT('',(0.0866025403784439,-0.64,0.15));
#21349=CARTESIAN_POINT('Origin',(0.,-0.4,-2.77555756156289E-17));
#21350=CARTESIAN_POINT('Origin',(0.,-0.64,-2.77555756156289E-17));
#21351=CARTESIAN_POINT('Origin',(0.,-1.,0.));
#21352=CARTESIAN_POINT('',(-0.1954,-1.,2.39295984553393E-17));
#21353=CARTESIAN_POINT('Origin',(0.,-1.,0.));
#21354=CARTESIAN_POINT('Origin',(0.3,0.4,0.));
#21355=CARTESIAN_POINT('',(-0.3,0.4,-3.67394039744206E-17));
#21356=CARTESIAN_POINT('Origin',(0.,0.4,0.));
#21357=CARTESIAN_POINT('Origin',(0.,0.375,0.));
#21358=CARTESIAN_POINT('',(-0.35,0.35,-4.28626379701573E-17));
#21359=CARTESIAN_POINT('Origin',(0.,0.35,0.));
#21360=CARTESIAN_POINT('',(-0.325,0.375,-3.9801020972289E-17));
#21361=CARTESIAN_POINT('Origin',(0.,0.19,0.));
#21362=CARTESIAN_POINT('',(-0.35,0.03,-4.28626379701574E-17));
#21363=CARTESIAN_POINT('Origin',(0.,0.03,0.));
#21364=CARTESIAN_POINT('',(-0.35,0.19,-4.28626379701574E-17));
#21365=CARTESIAN_POINT('Origin',(0.,0.0149999999999999,0.));
#21366=CARTESIAN_POINT('',(-0.32,-3.29597460435593E-17,-3.91886975727153E-17));
#21367=CARTESIAN_POINT('Origin',(0.,0.,0.));
#21368=CARTESIAN_POINT('',(-0.335,0.0149999999999999,-4.10256677714363E-17));
#21369=CARTESIAN_POINT('Origin',(0.22,0.,0.));
#21370=CARTESIAN_POINT('',(-0.22,-6.93889390390723E-18,-2.69422295812418E-17));
#21371=CARTESIAN_POINT('Origin',(0.,0.,0.));
#21372=CARTESIAN_POINT('Origin',(0.,-0.02,0.));
#21373=CARTESIAN_POINT('',(-0.1954,-0.0492,2.39295984553393E-17));
#21374=CARTESIAN_POINT('Origin',(0.,-0.0492,0.));
#21375=CARTESIAN_POINT('',(-0.21,-0.02,-2.57175827820944E-17));
#21376=CARTESIAN_POINT('Origin',(0.,-0.8,0.));
#21377=CARTESIAN_POINT('',(-0.1954,-0.8,-2.39295984553393E-17));
#34771=UNCERTAINTY_MEASURE_WITH_UNIT(LENGTH_MEASURE(0.001),#34852,
'DISTANCE_ACCURACY_VALUE',
'Maximum model space distance between geometric entities at asserted c
onnectivities');
#34797=UNCERTAINTY_MEASURE_WITH_UNIT(LENGTH_MEASURE(0.001),#34852,
'DISTANCE_ACCURACY_VALUE',
'Maximum model space distance between geometric entities at asserted c
onnectivities');
#34825=(
GEOMETRIC_REPRESENTATION_CONTEXT(3)
GLOBAL_UNCERTAINTY_ASSIGNED_CONTEXT((#34771))
GLOBAL_UNIT_ASSIGNED_CONTEXT((#34852,#34854,#34855))
REPRESENTATION_CONTEXT('','3D')
);
#34851=(
GEOMETRIC_REPRESENTATION_CONTEXT(3)
GLOBAL_UNCERTAINTY_ASSIGNED_CONTEXT((#34797))
GLOBAL_UNIT_ASSIGNED_CONTEXT((#34852,#34854,#34855))
REPRESENTATION_CONTEXT('','3D')
);
#34852=(
LENGTH_UNIT()
NAMED_UNIT(*)
SI_UNIT(.CENTI.,.METRE.)
);
#34854=(
NAMED_UNIT(*)
PLANE_ANGLE_UNIT()
SI_UNIT($,.RADIAN.)
);
#34855=(
NAMED_UNIT(*)
SI_UNIT($,.STERADIAN.)
SOLID_ANGLE_UNIT()
);
#34883=SHAPE_DEFINITION_REPRESENTATION(#34941,#35100);
#34941=PRODUCT_DEFINITION_SHAPE('',$,#35154);
#35100=SHAPE_REPRESENTATION('',(#14906),#34825);
#35126=PRODUCT_DEFINITION_CONTEXT('part definition',#35287,'design');
#35154=PRODUCT_DEFINITION('M4x10 Cap Screw','M4x10 Cap Screw',#35207,#35126);
#35207=PRODUCT_DEFINITION_FORMATION('',$,#35316);
#35287=APPLICATION_CONTEXT(
'Core Data for Automotive Mechanical Design Process');
#35288=PRODUCT_CONTEXT('part definition',#35287,'mechanical');
#35316=PRODUCT('M4x10 Cap Screw','M4x10 Cap Screw','M4x10 Cap Screw',(#35288));
#35412=COLOUR_RGB('Black',0.12,0.14,0.17);
#35413=FILL_AREA_STYLE_COLOUR('',#35412);
#35414=FILL_AREA_STYLE('',(#35413));
#35415=SURFACE_STYLE_FILL_AREA(#35414);
#35416=SURFACE_SIDE_STYLE('',(#35415));
#35417=SURFACE_STYLE_USAGE(.BOTH.,#35416);
#35418=PRESENTATION_STYLE_ASSIGNMENT((#35417));
ENDSEC;
END-ISO-10303-21;
